ISO-10303-21;
HEADER;
/* Generated by software containing ST-Developer
 * from STEP Tools, Inc. (www.steptools.com) 
 */

FILE_DESCRIPTION(
/* description */ ('Belt conveyor head drive unit'),
/* implementation_level */ '2;1');

FILE_NAME(
/* name */ 'M4x30 mounting screw.step',
/* time_stamp */ '2026-10-28T03:26:19-07:00',
/* author */ (''),
/* organization */ (''),
/* preprocessor_version */ 'ST-DEVELOPER v20.2',
/* originating_system */ 'Autodesk Translation Framework v15.17.0.0',
/* authorisation */ '');

FILE_SCHEMA (('AUTOMOTIVE_DESIGN { 1 0 10303 214 3 1 1 }'));
ENDSEC;

DATA;
#10=MECHANICAL_DESIGN_GEOMETRIC_PRESENTATION_REPRESENTATION('',(#887),#27069);
#11=ORIENTED_CLOSED_SHELL('',*,#13752,.F.);
#16=BREP_WITH_VOIDS('Body1',#13753,(#11));
#681=CONICAL_SURFACE('',#15340,0.325,0.785398163397448);
#682=CONICAL_SURFACE('',#15344,0.335,0.785398163397448);
#683=CONICAL_SURFACE('',#15348,0.21,0.463647609000806);
#684=CONICAL_SURFACE('',#15352,0.18,0.785398163397448);
#741=SHAPE_REPRESENTATION_RELATIONSHIP('SRR','None',#27386,#810);
#810=ADVANCED_BREP_SHAPE_REPRESENTATION('',(#16),#27028);
#887=STYLED_ITEM('',(#27804),#16);
#1160=FACE_BOUND('',#2943,.T.);
#1161=FACE_BOUND('',#2951,.T.);
#1454=PLANE('',#15324);
#1455=PLANE('',#15325);
#1456=PLANE('',#15326);
#1457=PLANE('',#15327);
#1458=PLANE('',#15328);
#1459=PLANE('',#15329);
#1460=PLANE('',#15330);
#1461=PLANE('',#15331);
#1462=PLANE('',#15332);
#1463=PLANE('',#15337);
#1464=PLANE('',#15338);
#1465=PLANE('',#15346);
#1986=FACE_OUTER_BOUND('',#2934,.T.);
#1987=FACE_OUTER_BOUND('',#2935,.T.);
#1988=FACE_OUTER_BOUND('',#2936,.T.);
#1989=FACE_OUTER_BOUND('',#2937,.T.);
#1990=FACE_OUTER_BOUND('',#2938,.T.);
#1991=FACE_OUTER_BOUND('',#2939,.T.);
#1992=FACE_OUTER_BOUND('',#2940,.T.);
#1993=FACE_OUTER_BOUND('',#2941,.T.);
#1994=FACE_OUTER_BOUND('',#2942,.T.);
#1995=FACE_OUTER_BOUND('',#2944,.T.);
#1996=FACE_OUTER_BOUND('',#2945,.T.);
#1997=FACE_OUTER_BOUND('',#2946,.T.);
#1998=FACE_OUTER_BOUND('',#2947,.T.);
#1999=FACE_OUTER_BOUND('',#2948,.T.);
#2000=FACE_OUTER_BOUND('',#2949,.T.);
#2001=FACE_OUTER_BOUND('',#2950,.T.);
#2002=FACE_OUTER_BOUND('',#2952,.T.);
#2003=FACE_OUTER_BOUND('',#2953,.T.);
#2004=FACE_OUTER_BOUND('',#2954,.T.);
#2934=EDGE_LOOP('',(#10484,#10485,#10486,#10487));
#2935=EDGE_LOOP('',(#10488,#10489,#10490,#10491));
#2936=EDGE_LOOP('',(#10492,#10493,#10494,#10495));
#2937=EDGE_LOOP('',(#10496,#10497,#10498,#10499));
#2938=EDGE_LOOP('',(#10500,#10501,#10502,#10503));
#2939=EDGE_LOOP('',(#10504,#10505,#10506,#10507));
#2940=EDGE_LOOP('',(#10508,#10509,#10510,#10511,#10512,#10513));
#2941=EDGE_LOOP('',(#10514,#10515,#10516,#10517,#10518,#10519));
#2942=EDGE_LOOP('',(#10520));
#2943=EDGE_LOOP('',(#10521));
#2944=EDGE_LOOP('',(#10522,#10523,#10524,#10525));
#2945=EDGE_LOOP('',(#10526));
#2946=EDGE_LOOP('',(#10527));
#2947=EDGE_LOOP('',(#10528,#10529,#10530,#10531));
#2948=EDGE_LOOP('',(#10532,#10533,#10534,#10535));
#2949=EDGE_LOOP('',(#10536,#10537,#10538,#10539));
#2950=EDGE_LOOP('',(#10540));
#2951=EDGE_LOOP('',(#10541));
#2952=EDGE_LOOP('',(#10542,#10543,#10544,#10545));
#2953=EDGE_LOOP('',(#10546,#10547,#10548,#10549));
#2954=EDGE_LOOP('',(#10550,#10551,#10552,#10553));
#3875=LINE('',#22986,#4667);
#3876=LINE('',#22988,#4668);
#3877=LINE('',#22990,#4669);
#3878=LINE('',#22991,#4670);
#3879=LINE('',#22994,#4671);
#3880=LINE('',#22996,#4672);
#3881=LINE('',#22997,#4673);
#3882=LINE('',#23000,#4674);
#3883=LINE('',#23002,#4675);
#3884=LINE('',#23003,#4676);
#3885=LINE('',#23006,#4677);
#3886=LINE('',#23008,#4678);
#3887=LINE('',#23009,#4679);
#3888=LINE('',#23012,#4680);
#3889=LINE('',#23014,#4681);
#3890=LINE('',#23015,#4682);
#3891=LINE('',#23017,#4683);
#3892=LINE('',#23018,#4684);
#3893=LINE('',#23028,#4685);
#3894=LINE('',#23037,#4686);
#3895=LINE('',#23041,#4687);
#3896=LINE('',#23045,#4688);
#3897=LINE('',#23052,#4689);
#3898=LINE('',#23056,#4690);
#3899=LINE('',#23058,#4691);
#4667=VECTOR('',#18337,1.);
#4668=VECTOR('',#18338,1.);
#4669=VECTOR('',#18339,1.);
#4670=VECTOR('',#18340,1.);
#4671=VECTOR('',#18343,1.);
#4672=VECTOR('',#18344,1.);
#4673=VECTOR('',#18345,1.);
#4674=VECTOR('',#18348,1.);
#4675=VECTOR('',#18349,1.);
#4676=VECTOR('',#18350,1.);
#4677=VECTOR('',#18353,1.);
#4678=VECTOR('',#18354,1.);
#4679=VECTOR('',#18355,1.);
#4680=VECTOR('',#18358,1.);
#4681=VECTOR('',#18359,1.);
#4682=VECTOR('',#18360,1.);
#4683=VECTOR('',#18363,1.);
#4684=VECTOR('',#18364,1.);
#4685=VECTOR('',#18377,0.2);
#4686=VECTOR('',#18390,0.325);
#4687=VECTOR('',#18395,0.35);
#4688=VECTOR('',#18400,0.335);
#4689=VECTOR('',#18409,0.21);
#4690=VECTOR('',#18414,0.2);
#4691=VECTOR('',#18417,0.18);
#5450=CIRCLE('',#15333,0.2);
#5451=CIRCLE('',#15334,0.16);
#5452=CIRCLE('',#15336,0.2);
#5453=CIRCLE('',#15339,0.3);
#5454=CIRCLE('',#15341,0.35);
#5455=CIRCLE('',#15343,0.35);
#5456=CIRCLE('',#15345,0.32);
#5457=CIRCLE('',#15347,0.22);
#5458=CIRCLE('',#15349,0.1954);
#5459=CIRCLE('',#15351,0.1954);
#6471=VERTEX_POINT('',#22984);
#6472=VERTEX_POINT('',#22985);
#6473=VERTEX_POINT('',#22987);
#6474=VERTEX_POINT('',#22989);
#6475=VERTEX_POINT('',#22993);
#6476=VERTEX_POINT('',#22995);
#6477=VERTEX_POINT('',#22999);
#6478=VERTEX_POINT('',#23001);
#6479=VERTEX_POINT('',#23005);
#6480=VERTEX_POINT('',#23007);
#6481=VERTEX_POINT('',#23011);
#6482=VERTEX_POINT('',#23013);
#6483=VERTEX_POINT('',#23022);
#6484=VERTEX_POINT('',#23024);
#6485=VERTEX_POINT('',#23027);
#6486=VERTEX_POINT('',#23032);
#6487=VERTEX_POINT('',#23035);
#6488=VERTEX_POINT('',#23039);
#6489=VERTEX_POINT('',#23043);
#6490=VERTEX_POINT('',#23047);
#6491=VERTEX_POINT('',#23050);
#6492=VERTEX_POINT('',#23054);
#7934=EDGE_CURVE('',#6471,#6472,#3875,.T.);
#7935=EDGE_CURVE('',#6472,#6473,#3876,.T.);
#7936=EDGE_CURVE('',#6473,#6474,#3877,.T.);
#7937=EDGE_CURVE('',#6471,#6474,#3878,.T.);
#7938=EDGE_CURVE('',#6472,#6475,#3879,.T.);
#7939=EDGE_CURVE('',#6475,#6476,#3880,.T.);
#7940=EDGE_CURVE('',#6476,#6473,#3881,.T.);
#7941=EDGE_CURVE('',#6475,#6477,#3882,.T.);
#7942=EDGE_CURVE('',#6477,#6478,#3883,.T.);
#7943=EDGE_CURVE('',#6478,#6476,#3884,.T.);
#7944=EDGE_CURVE('',#6477,#6479,#3885,.T.);
#7945=EDGE_CURVE('',#6479,#6480,#3886,.T.);
#7946=EDGE_CURVE('',#6480,#6478,#3887,.T.);
#7947=EDGE_CURVE('',#6479,#6481,#3888,.T.);
#7948=EDGE_CURVE('',#6481,#6482,#3889,.T.);
#7949=EDGE_CURVE('',#6482,#6480,#3890,.T.);
#7950=EDGE_CURVE('',#6481,#6471,#3891,.T.);
#7951=EDGE_CURVE('',#6474,#6482,#3892,.T.);
#7952=EDGE_CURVE('',#6483,#6483,#5450,.T.);
#7953=EDGE_CURVE('',#6484,#6484,#5451,.T.);
#7954=EDGE_CURVE('',#6483,#6485,#3893,.T.);
#7955=EDGE_CURVE('',#6485,#6485,#5452,.T.);
#7956=EDGE_CURVE('',#6486,#6486,#5453,.T.);
#7957=EDGE_CURVE('',#6487,#6487,#5454,.T.);
#7958=EDGE_CURVE('',#6487,#6486,#3894,.T.);
#7959=EDGE_CURVE('',#6488,#6488,#5455,.T.);
#7960=EDGE_CURVE('',#6488,#6487,#3895,.T.);
#7961=EDGE_CURVE('',#6489,#6489,#5456,.T.);
#7962=EDGE_CURVE('',#6489,#6488,#3896,.T.);
#7963=EDGE_CURVE('',#6490,#6490,#5457,.T.);
#7964=EDGE_CURVE('',#6491,#6491,#5458,.F.);
#7965=EDGE_CURVE('',#6491,#6490,#3897,.T.);
#7966=EDGE_CURVE('',#6492,#6492,#5459,.F.);
#7967=EDGE_CURVE('',#6492,#6491,#3898,.T.);
#7968=EDGE_CURVE('',#6484,#6492,#3899,.T.);
#10484=ORIENTED_EDGE('',*,*,#7934,.T.);
#10485=ORIENTED_EDGE('',*,*,#7935,.T.);
#10486=ORIENTED_EDGE('',*,*,#7936,.T.);
#10487=ORIENTED_EDGE('',*,*,#7937,.F.);
#10488=ORIENTED_EDGE('',*,*,#7938,.T.);
#10489=ORIENTED_EDGE('',*,*,#7939,.T.);
#10490=ORIENTED_EDGE('',*,*,#7940,.T.);
#10491=ORIENTED_EDGE('',*,*,#7935,.F.);
#10492=ORIENTED_EDGE('',*,*,#7941,.T.);
#10493=ORIENTED_EDGE('',*,*,#7942,.T.);
#10494=ORIENTED_EDGE('',*,*,#7943,.T.);
#10495=ORIENTED_EDGE('',*,*,#7939,.F.);
#10496=ORIENTED_EDGE('',*,*,#7944,.T.);
#10497=ORIENTED_EDGE('',*,*,#7945,.T.);
#10498=ORIENTED_EDGE('',*,*,#7946,.T.);
#10499=ORIENTED_EDGE('',*,*,#7942,.F.);
#10500=ORIENTED_EDGE('',*,*,#7947,.T.);
#10501=ORIENTED_EDGE('',*,*,#7948,.T.);
#10502=ORIENTED_EDGE('',*,*,#7949,.T.);
#10503=ORIENTED_EDGE('',*,*,#7945,.F.);
#10504=ORIENTED_EDGE('',*,*,#7950,.T.);
#10505=ORIENTED_EDGE('',*,*,#7937,.T.);
#10506=ORIENTED_EDGE('',*,*,#7951,.T.);
#10507=ORIENTED_EDGE('',*,*,#7948,.F.);
#10508=ORIENTED_EDGE('',*,*,#7950,.F.);
#10509=ORIENTED_EDGE('',*,*,#7947,.F.);
#10510=ORIENTED_EDGE('',*,*,#7944,.F.);
#10511=ORIENTED_EDGE('',*,*,#7941,.F.);
#10512=ORIENTED_EDGE('',*,*,#7938,.F.);
#10513=ORIENTED_EDGE('',*,*,#7934,.F.);
#10514=ORIENTED_EDGE('',*,*,#7951,.F.);
#10515=ORIENTED_EDGE('',*,*,#7936,.F.);
#10516=ORIENTED_EDGE('',*,*,#7940,.F.);
#10517=ORIENTED_EDGE('',*,*,#7943,.F.);
#10518=ORIENTED_EDGE('',*,*,#7946,.F.);
#10519=ORIENTED_EDGE('',*,*,#7949,.F.);
#10520=ORIENTED_EDGE('',*,*,#7952,.T.);
#10521=ORIENTED_EDGE('',*,*,#7953,.T.);
#10522=ORIENTED_EDGE('',*,*,#7952,.F.);
#10523=ORIENTED_EDGE('',*,*,#7954,.T.);
#10524=ORIENTED_EDGE('',*,*,#7955,.T.);
#10525=ORIENTED_EDGE('',*,*,#7954,.F.);
#10526=ORIENTED_EDGE('',*,*,#7955,.F.);
#10527=ORIENTED_EDGE('',*,*,#7956,.F.);
#10528=ORIENTED_EDGE('',*,*,#7957,.F.);
#10529=ORIENTED_EDGE('',*,*,#7958,.T.);
#10530=ORIENTED_EDGE('',*,*,#7956,.T.);
#10531=ORIENTED_EDGE('',*,*,#7958,.F.);
#10532=ORIENTED_EDGE('',*,*,#7959,.F.);
#10533=ORIENTED_EDGE('',*,*,#7960,.T.);
#10534=ORIENTED_EDGE('',*,*,#7957,.T.);
#10535=ORIENTED_EDGE('',*,*,#7960,.F.);
#10536=ORIENTED_EDGE('',*,*,#7961,.F.);
#10537=ORIENTED_EDGE('',*,*,#7962,.T.);
#10538=ORIENTED_EDGE('',*,*,#7959,.T.);
#10539=ORIENTED_EDGE('',*,*,#7962,.F.);
#10540=ORIENTED_EDGE('',*,*,#7961,.T.);
#10541=ORIENTED_EDGE('',*,*,#7963,.F.);
#10542=ORIENTED_EDGE('',*,*,#7964,.F.);
#10543=ORIENTED_EDGE('',*,*,#7965,.T.);
#10544=ORIENTED_EDGE('',*,*,#7963,.T.);
#10545=ORIENTED_EDGE('',*,*,#7965,.F.);
#10546=ORIENTED_EDGE('',*,*,#7966,.F.);
#10547=ORIENTED_EDGE('',*,*,#7967,.T.);
#10548=ORIENTED_EDGE('',*,*,#7964,.T.);
#10549=ORIENTED_EDGE('',*,*,#7967,.F.);
#10550=ORIENTED_EDGE('',*,*,#7953,.F.);
#10551=ORIENTED_EDGE('',*,*,#7968,.T.);
#10552=ORIENTED_EDGE('',*,*,#7966,.T.);
#10553=ORIENTED_EDGE('',*,*,#7968,.F.);
#12686=CYLINDRICAL_SURFACE('',#15335,0.2);
#12687=CYLINDRICAL_SURFACE('',#15342,0.35);
#12688=CYLINDRICAL_SURFACE('',#15350,0.1954);
#13265=ADVANCED_FACE('',(#1986),#1454,.F.);
#13266=ADVANCED_FACE('',(#1987),#1455,.F.);
#13267=ADVANCED_FACE('',(#1988),#1456,.F.);
#13268=ADVANCED_FACE('',(#1989),#1457,.F.);
#13269=ADVANCED_FACE('',(#1990),#1458,.F.);
#13270=ADVANCED_FACE('',(#1991),#1459,.F.);
#13271=ADVANCED_FACE('',(#1992),#1460,.F.);
#13272=ADVANCED_FACE('',(#1993),#1461,.F.);
#13273=ADVANCED_FACE('',(#1994,#1160),#1462,.T.);
#13274=ADVANCED_FACE('',(#1995),#12686,.T.);
#13275=ADVANCED_FACE('',(#1996),#1463,.F.);
#13276=ADVANCED_FACE('',(#1997),#1464,.T.);
#13277=ADVANCED_FACE('',(#1998),#681,.T.);
#13278=ADVANCED_FACE('',(#1999),#12687,.T.);
#13279=ADVANCED_FACE('',(#2000),#682,.T.);
#13280=ADVANCED_FACE('',(#2001,#1161),#1465,.T.);
#13281=ADVANCED_FACE('',(#2002),#683,.T.);
#13282=ADVANCED_FACE('',(#2003),#12688,.T.);
#13283=ADVANCED_FACE('',(#2004),#684,.T.);
#13752=CLOSED_SHELL('',(#13265,#13266,#13267,#13268,#13269,#13270,#13271,
#13272));
#13753=CLOSED_SHELL('',(#13273,#13274,#13275,#13276,#13277,#13278,#13279,
#13280,#13281,#13282,#13283));
#15323=AXIS2_PLACEMENT_3D('',#22982,#18333,#18334);
#15324=AXIS2_PLACEMENT_3D('',#22983,#18335,#18336);
#15325=AXIS2_PLACEMENT_3D('',#22992,#18341,#18342);
#15326=AXIS2_PLACEMENT_3D('',#22998,#18346,#18347);
#15327=AXIS2_PLACEMENT_3D('',#23004,#18351,#18352);
#15328=AXIS2_PLACEMENT_3D('',#23010,#18356,#18357);
#15329=AXIS2_PLACEMENT_3D('',#23016,#18361,#18362);
#15330=AXIS2_PLACEMENT_3D('',#23019,#18365,#18366);
#15331=AXIS2_PLACEMENT_3D('',#23020,#18367,#18368);
#15332=AXIS2_PLACEMENT_3D('',#23021,#18369,#18370);
#15333=AXIS2_PLACEMENT_3D('',#23023,#18371,#18372);
#15334=AXIS2_PLACEMENT_3D('',#23025,#18373,#18374);
#15335=AXIS2_PLACEMENT_3D('',#23026,#18375,#18376);
#15336=AXIS2_PLACEMENT_3D('',#23029,#18378,#18379);
#15337=AXIS2_PLACEMENT_3D('',#23030,#18380,#18381);
#15338=AXIS2_PLACEMENT_3D('',#23031,#18382,#18383);
#15339=AXIS2_PLACEMENT_3D('',#23033,#18384,#18385);
#15340=AXIS2_PLACEMENT_3D('',#23034,#18386,#18387);
#15341=AXIS2_PLACEMENT_3D('',#23036,#18388,#18389);
#15342=AXIS2_PLACEMENT_3D('',#23038,#18391,#18392);
#15343=AXIS2_PLACEMENT_3D('',#23040,#18393,#18394);
#15344=AXIS2_PLACEMENT_3D('',#23042,#18396,#18397);
#15345=AXIS2_PLACEMENT_3D('',#23044,#18398,#18399);
#15346=AXIS2_PLACEMENT_3D('',#23046,#18401,#18402);
#15347=AXIS2_PLACEMENT_3D('',#23048,#18403,#18404);
#15348=AXIS2_PLACEMENT_3D('',#23049,#18405,#18406);
#15349=AXIS2_PLACEMENT_3D('',#23051,#18407,#18408);
#15350=AXIS2_PLACEMENT_3D('',#23053,#18410,#18411);
#15351=AXIS2_PLACEMENT_3D('',#23055,#18412,#18413);
#15352=AXIS2_PLACEMENT_3D('',#23057,#18415,#18416);
#18333=DIRECTION('axis',(0.,0.,1.));
#18334=DIRECTION('refdir',(1.,0.,0.));
#18335=DIRECTION('center_axis',(0.866025403784439,0.,-0.5));
#18336=DIRECTION('ref_axis',(0.5,0.,0.866025403784439));
#18337=DIRECTION('',(-0.5,0.,-0.866025403784439));
#18338=DIRECTION('',(0.,-1.,0.));
#18339=DIRECTION('',(0.5,0.,0.866025403784439));
#18340=DIRECTION('',(0.,-1.,0.));
#18341=DIRECTION('center_axis',(1.60246890531964E-16,0.,-1.));
#18342=DIRECTION('ref_axis',(1.,0.,1.60246890531964E-16));
#18343=DIRECTION('',(-1.,0.,-1.60246890531964E-16));
#18344=DIRECTION('',(0.,-1.,0.));
#18345=DIRECTION('',(1.,0.,1.60246890531964E-16));
#18346=DIRECTION('center_axis',(-0.866025403784439,0.,-0.5));
#18347=DIRECTION('ref_axis',(0.5,0.,-0.866025403784439));
#18348=DIRECTION('',(-0.5,0.,0.866025403784439));
#18349=DIRECTION('',(0.,-1.,0.));
#18350=DIRECTION('',(0.5,0.,-0.866025403784439));
#18351=DIRECTION('center_axis',(-0.866025403784439,0.,0.5));
#18352=DIRECTION('ref_axis',(-0.5,0.,-0.866025403784439));
#18353=DIRECTION('',(0.5,0.,0.866025403784439));
#18354=DIRECTION('',(0.,-1.,0.));
#18355=DIRECTION('',(-0.5,0.,-0.866025403784439));
#18356=DIRECTION('center_axis',(-1.60246890531964E-16,0.,1.));
#18357=DIRECTION('ref_axis',(-1.,0.,-1.60246890531964E-16));
#18358=DIRECTION('',(1.,0.,1.60246890531964E-16));
#18359=DIRECTION('',(0.,-1.,0.));
#18360=DIRECTION('',(-1.,0.,-1.60246890531964E-16));
#18361=DIRECTION('center_axis',(0.866025403784439,0.,0.5));
#18362=DIRECTION('ref_axis',(-0.5,0.,0.866025403784439));
#18363=DIRECTION('',(0.5,0.,-0.866025403784439));
#18364=DIRECTION('',(-0.5,0.,0.866025403784439));
#18365=DIRECTION('center_axis',(0.,1.,0.));
#18366=DIRECTION('ref_axis',(1.,0.,0.));
#18367=DIRECTION('center_axis',(0.,-1.,0.));
#18368=DIRECTION('ref_axis',(0.,0.,-1.));
#18369=DIRECTION('center_axis',(0.,1.,0.));
#18370=DIRECTION('ref_axis',(1.,0.,0.));
#18371=DIRECTION('center_axis',(0.,1.,0.));
#18372=DIRECTION('ref_axis',(1.,0.,0.));
#18373=DIRECTION('center_axis',(0.,-1.,0.));
#18374=DIRECTION('ref_axis',(1.,0.,0.));
#18375=DIRECTION('center_axis',(0.,1.,0.));
#18376=DIRECTION('ref_axis',(1.,0.,0.));
#18377=DIRECTION('',(0.,-1.,0.));
#18378=DIRECTION('center_axis',(0.,1.,0.));
#18379=DIRECTION('ref_axis',(1.,0.,0.));
#18380=DIRECTION('center_axis',(0.,1.,0.));
#18381=DIRECTION('ref_axis',(1.,0.,0.));
#18382=DIRECTION('center_axis',(0.,1.,0.));
#18383=DIRECTION('ref_axis',(0.,0.,1.));
#18384=DIRECTION('center_axis',(0.,-1.,0.));
#18385=DIRECTION('ref_axis',(1.,0.,0.));
#18386=DIRECTION('center_axis',(0.,-1.,0.));
#18387=DIRECTION('ref_axis',(1.,0.,0.));
#18388=DIRECTION('center_axis',(0.,-1.,0.));
#18389=DIRECTION('ref_axis',(1.,0.,0.));
#18390=DIRECTION('',(0.707106781186547,0.707106781186548,8.65956056235493E-17));
#18391=DIRECTION('center_axis',(0.,-1.,0.));
#18392=DIRECTION('ref_axis',(1.,0.,0.));
#18393=DIRECTION('center_axis',(0.,-1.,0.));
#18394=DIRECTION('ref_axis',(1.,0.,0.));
#18395=DIRECTION('',(0.,1.,0.));
#18396=DIRECTION('center_axis',(0.,1.,0.));
#18397=DIRECTION('ref_axis',(1.,0.,0.));
#18398=DIRECTION('center_axis',(0.,-1.,0.));
#18399=DIRECTION('ref_axis',(1.,0.,0.));
#18400=DIRECTION('',(-0.707106781186547,0.707106781186548,-8.65956056235493E-17));
#18401=DIRECTION('center_axis',(0.,-1.,0.));
#18402=DIRECTION('ref_axis',(0.,0.,-1.));
#18403=DIRECTION('center_axis',(0.,-1.,0.));
#18404=DIRECTION('ref_axis',(1.,0.,0.));
#18405=DIRECTION('center_axis',(0.,1.,0.));
#18406=DIRECTION('ref_axis',(1.,0.,0.));
#18407=DIRECTION('center_axis',(0.,1.,0.));
#18408=DIRECTION('ref_axis',(1.,0.,0.));
#18409=DIRECTION('',(-0.447213595499958,0.894427190999916,-5.47678698264203E-17));
#18410=DIRECTION('center_axis',(0.,-1.,0.));
#18411=DIRECTION('ref_axis',(1.,0.,0.));
#18412=DIRECTION('center_axis',(0.,1.,0.));
#18413=DIRECTION('ref_axis',(1.,0.,0.));
#18414=DIRECTION('',(0.,1.,0.));
#18415=DIRECTION('center_axis',(0.,1.,0.));
#18416=DIRECTION('ref_axis',(1.,0.,0.));
#18417=DIRECTION('',(-0.707106781186547,0.707106781186548,-8.65956056235493E-17));
#22982=CARTESIAN_POINT('',(0.,0.,0.));
#22983=CARTESIAN_POINT('Origin',(0.0866025403784439,-0.4,-0.15));
#22984=CARTESIAN_POINT('',(0.173205080756888,-0.4,0.));
#22985=CARTESIAN_POINT('',(0.0866025403784439,-0.4,-0.15));
#22986=CARTESIAN_POINT('',(0.173205080756888,-0.4,0.));
#22987=CARTESIAN_POINT('',(0.0866025403784439,-0.64,-0.15));
#22988=CARTESIAN_POINT('',(0.0866025403784439,-0.4,-0.15));
#22989=CARTESIAN_POINT('',(0.173205080756888,-0.64,0.));
#22990=CARTESIAN_POINT('',(0.173205080756888,-0.64,0.));
#22991=CARTESIAN_POINT('',(0.173205080756888,-0.4,0.));
#22992=CARTESIAN_POINT('Origin',(-0.0866025403784438,-0.4,-0.15));
#22993=CARTESIAN_POINT('',(-0.0866025403784438,-0.4,-0.15));
#22994=CARTESIAN_POINT('',(0.0866025403784439,-0.4,-0.15));
#22995=CARTESIAN_POINT('',(-0.0866025403784438,-0.64,-0.15));
#22996=CARTESIAN_POINT('',(-0.0866025403784438,-0.4,-0.15));
#22997=CARTESIAN_POINT('',(0.0866025403784439,-0.64,-0.15));
#22998=CARTESIAN_POINT('Origin',(-0.173205080756888,-0.4,-2.77555756156289E-17));
#22999=CARTESIAN_POINT('',(-0.173205080756888,-0.4,-2.12115047744981E-17));
#23000=CARTESIAN_POINT('',(-0.0866025403784438,-0.4,-0.15));
#23001=CARTESIAN_POINT('',(-0.173205080756888,-0.64,-2.77555756156289E-17));
#23002=CARTESIAN_POINT('',(-0.173205080756888,-0.4,-2.12115047744981E-17));
#23003=CARTESIAN_POINT('',(-0.0866025403784438,-0.64,-0.15));
#23004=CARTESIAN_POINT('Origin',(-0.0866025403784439,-0.4,0.15));
#23005=CARTESIAN_POINT('',(-0.0866025403784439,-0.4,0.15));
#23006=CARTESIAN_POINT('',(-0.173205080756888,-0.4,-2.12115047744981E-17));
#23007=CARTESIAN_POINT('',(-0.0866025403784439,-0.64,0.15));
#23008=CARTESIAN_POINT('',(-0.0866025403784439,-0.4,0.15));
#23009=CARTESIAN_POINT('',(-0.173205080756888,-0.64,-2.12115047744981E-17));
#23010=CARTESIAN_POINT('Origin',(0.0866025403784439,-0.4,0.15));
#23011=CARTESIAN_POINT('',(0.0866025403784439,-0.4,0.15));
#23012=CARTESIAN_POINT('',(-0.0866025403784439,-0.4,0.15));
#23013=CARTESIAN_POINT('',(0.0866025403784439,-0.64,0.15));
#23014=CARTESIAN_POINT('',(0.0866025403784439,-0.4,0.15));
#23015=CARTESIAN_POINT('',(-0.0866025403784439,-0.64,0.15));
#23016=CARTESIAN_POINT('Origin',(0.173205080756888,-0.4,0.));
#23017=CARTESIAN_POINT('',(0.0866025403784439,-0.4,0.15));
#23018=CARTESIAN_POINT('',(0.0866025403784439,-0.64,0.15));
#23019=CARTESIAN_POINT('Origin',(0.,-0.4,-2.77555756156289E-17));
#23020=CARTESIAN_POINT('Origin',(0.,-0.64,-2.77555756156289E-17));
#23021=CARTESIAN_POINT('Origin',(0.,-1.6,0.));
#23022=CARTESIAN_POINT('',(-0.2,-1.6,2.44929359829471E-17));
#23023=CARTESIAN_POINT('Origin',(0.,-1.6,0.));
#23024=CARTESIAN_POINT('',(-0.16,-1.6,-1.95943487863577E-17));
#23025=CARTESIAN_POINT('Origin',(0.,-1.6,0.));
#23026=CARTESIAN_POINT('Origin',(0.,-3.,0.));
#23027=CARTESIAN_POINT('',(-0.2,-3.,2.44929359829471E-17));
#23028=CARTESIAN_POINT('',(-0.2,-3.,2.44929359829471E-17));
#23029=CARTESIAN_POINT('Origin',(0.,-3.,0.));
#23030=CARTESIAN_POINT('Origin',(0.,-3.,0.));
#23031=CARTESIAN_POINT('Origin',(0.3,0.4,0.));
#23032=CARTESIAN_POINT('',(-0.3,0.4,-3.67394039744206E-17));
#23033=CARTESIAN_POINT('Origin',(0.,0.4,0.));
#23034=CARTESIAN_POINT('Origin',(0.,0.375,0.));
#23035=CARTESIAN_POINT('',(-0.35,0.35,-4.28626379701573E-17));
#23036=CARTESIAN_POINT('Origin',(0.,0.35,0.));
#23037=CARTESIAN_POINT('',(-0.325,0.375,-3.9801020972289E-17));
#23038=CARTESIAN_POINT('Origin',(0.,0.19,0.));
#23039=CARTESIAN_POINT('',(-0.35,0.03,-4.28626379701574E-17));
#23040=CARTESIAN_POINT('Origin',(0.,0.03,0.));
#23041=CARTESIAN_POINT('',(-0.35,0.19,-4.28626379701574E-17));
#23042=CARTESIAN_POINT('Origin',(0.,0.0149999999999999,0.));
#23043=CARTESIAN_POINT('',(-0.32,-3.29597460435593E-17,-3.91886975727153E-17));
#23044=CARTESIAN_POINT('Origin',(0.,0.,0.));
#23045=CARTESIAN_POINT('',(-0.335,0.0149999999999999,-4.10256677714363E-17));
#23046=CARTESIAN_POINT('Origin',(0.22,0.,0.));
#23047=CARTESIAN_POINT('',(-0.22,-6.93889390390723E-18,-2.69422295812418E-17));
#23048=CARTESIAN_POINT('Origin',(0.,0.,0.));
#23049=CARTESIAN_POINT('Origin',(0.,-0.02,0.));
#23050=CARTESIAN_POINT('',(-0.1954,-0.0492,2.39295984553393E-17));
#23051=CARTESIAN_POINT('Origin',(0.,-0.0492,0.));
#23052=CARTESIAN_POINT('',(-0.21,-0.02,-2.57175827820944E-17));
#23053=CARTESIAN_POINT('Origin',(0.,-0.8,0.));
#23054=CARTESIAN_POINT('',(-0.1954,-1.5646,2.39295984553393E-17));
#23055=CARTESIAN_POINT('Origin',(0.,-1.5646,0.));
#23056=CARTESIAN_POINT('',(-0.1954,-0.8,-2.39295984553393E-17));
#23057=CARTESIAN_POINT('Origin',(0.,-1.58,0.));
#23058=CARTESIAN_POINT('',(-0.18,-1.58,-2.20436423846524E-17));
#26951=UNCERTAINTY_MEASURE_WITH_UNIT(LENGTH_MEASURE(0.001),#27070,
'DISTANCE_ACCURACY_VALUE',
'Maximum model space distance between geometric entities at asserted c
onnectivities');
#26992=UNCERTAINTY_MEASURE_WITH_UNIT(LENGTH_MEASURE(0.001),#27070,
'DISTANCE_ACCURACY_VALUE',
'Maximum model space distance between geometric entities at asserted c
onnectivities');
#27028=(
GEOMETRIC_REPRESENTATION_CONTEXT(3)
GLOBAL_UNCERTAINTY_ASSIGNED_CONTEXT((#26951))
GLOBAL_UNIT_ASSIGNED_CONTEXT((#27070,#27072,#27073))
REPRESENTATION_CONTEXT('','3D')
);
#27069=(
GEOMETRIC_REPRESENTATION_CONTEXT(3)
GLOBAL_UNCERTAINTY_ASSIGNED_CONTEXT((#26992))
GLOBAL_UNIT_ASSIGNED_CONTEXT((#27070,#27072,#27073))
REPRESENTATION_CONTEXT('','3D')
);
#27070=(
LENGTH_UNIT()
NAMED_UNIT(*)
SI_UNIT(.CENTI.,.METRE.)
);
#27072=(
NAMED_UNIT(*)
PLANE_ANGLE_UNIT()
SI_UNIT($,.RADIAN.)
);
#27073=(
NAMED_UNIT(*)
SI_UNIT($,.STERADIAN.)
SOLID_ANGLE_UNIT()
);
#27109=SHAPE_DEFINITION_REPRESENTATION(#27190,#27386);
#27190=PRODUCT_DEFINITION_SHAPE('',$,#27463);
#27386=SHAPE_REPRESENTATION('',(#15323),#27028);
#27427=PRODUCT_DEFINITION_CONTEXT('part definition',#27657,'design');
#27463=PRODUCT_DEFINITION('M4x30 mounting screw','M4x30 mounting screw',
#27539,#27427);
#27539=PRODUCT_DEFINITION_FORMATION('',$,#27694);
#27657=APPLICATION_CONTEXT(
'Core Data for Automotive Mechanical Design Process');
#27658=PRODUCT_CONTEXT('part definition',#27657,'mechanical');
#27694=PRODUCT('M4x30 mounting screw','M4x30 mounting screw',
'M4x30 mounting screw',(#27658));
#27798=COLOUR_RGB('Black',0.12,0.14,0.17);
#27799=FILL_AREA_STYLE_COLOUR('',#27798);
#27800=FILL_AREA_STYLE('',(#27799));
#27801=SURFACE_STYLE_FILL_AREA(#27800);
#27802=SURFACE_SIDE_STYLE('',(#27801));
#27803=SURFACE_STYLE_USAGE(.BOTH.,#27802);
#27804=PRESENTATION_STYLE_ASSIGNMENT((#27803));
ENDSEC;
END-ISO-10303-21;
